ISO-10303-21;
HEADER;
/* Generated by software containing ST-Developer
 * from STEP Tools, Inc. (www.steptools.com) 
 */

FILE_DESCRIPTION(
/* description */ ('Four-wheel beam trolley'),
/* implementation_level */ '2;1');

FILE_NAME(
/* name */ 'Cap Screw - M8x30.step',
/* time_stamp */ '2026-10-29T16:22:06-07:00',
/* author */ (''),
/* organization */ (''),
/* preprocessor_version */ 'ST-DEVELOPER v20.2',
/* originating_system */ 'Autodesk Translation Framework v15.17.0.0',
/* authorisation */ '');

FILE_SCHEMA (('AUTOMOTIVE_DESIGN { 1 0 10303 214 3 1 1 }'));
ENDSEC;

DATA;
#10=MECHANICAL_DESIGN_GEOMETRIC_PRESENTATION_REPRESENTATION('',(#282),#4777);
#229=ORIENTED_CLOSED_SHELL('',*,#2370,.F.);
#231=CONICAL_SURFACE('',#2647,0.625,0.785398163397448);
#232=CONICAL_SURFACE('',#2651,0.635,0.785398163397449);
#233=CONICAL_SURFACE('',#2655,0.41,0.463647609000806);
#234=CONICAL_SURFACE('',#2659,0.36,0.785398163397448);
#242=BREP_WITH_VOIDS('Body1',#2369,(#229));
#248=SHAPE_REPRESENTATION_RELATIONSHIP('SRR','None',#4877,#265);
#265=ADVANCED_BREP_SHAPE_REPRESENTATION('',(#242),#4762);
#282=STYLED_ITEM('',(#5063),#242);
#340=FACE_BOUND('',#645,.T.);
#388=PLANE('',#2645);
#389=PLANE('',#2653);
#390=PLANE('',#2661);
#391=PLANE('',#2662);
#392=PLANE('',#2663);
#393=PLANE('',#2664);
#394=PLANE('',#2665);
#395=PLANE('',#2666);
#396=PLANE('',#2667);
#397=PLANE('',#2668);
#398=PLANE('',#2669);
#477=FACE_OUTER_BOUND('',#640,.T.);
#478=FACE_OUTER_BOUND('',#641,.T.);
#479=FACE_OUTER_BOUND('',#642,.T.);
#480=FACE_OUTER_BOUND('',#643,.T.);
#481=FACE_OUTER_BOUND('',#644,.T.);
#482=FACE_OUTER_BOUND('',#646,.T.);
#483=FACE_OUTER_BOUND('',#647,.T.);
#484=FACE_OUTER_BOUND('',#648,.T.);
#485=FACE_OUTER_BOUND('',#649,.T.);
#486=FACE_OUTER_BOUND('',#650,.T.);
#487=FACE_OUTER_BOUND('',#651,.T.);
#488=FACE_OUTER_BOUND('',#652,.T.);
#489=FACE_OUTER_BOUND('',#653,.T.);
#490=FACE_OUTER_BOUND('',#654,.T.);
#491=FACE_OUTER_BOUND('',#655,.T.);
#492=FACE_OUTER_BOUND('',#656,.T.);
#493=FACE_OUTER_BOUND('',#657,.T.);
#640=EDGE_LOOP('',(#1763));
#641=EDGE_LOOP('',(#1764,#1765,#1766,#1767));
#642=EDGE_LOOP('',(#1768,#1769,#1770,#1771));
#643=EDGE_LOOP('',(#1772,#1773,#1774,#1775));
#644=EDGE_LOOP('',(#1776));
#645=EDGE_LOOP('',(#1777));
#646=EDGE_LOOP('',(#1778,#1779,#1780,#1781));
#647=EDGE_LOOP('',(#1782,#1783,#1784,#1785));
#648=EDGE_LOOP('',(#1786,#1787,#1788,#1789));
#649=EDGE_LOOP('',(#1790));
#650=EDGE_LOOP('',(#1791,#1792,#1793,#1794));
#651=EDGE_LOOP('',(#1795,#1796,#1797,#1798));
#652=EDGE_LOOP('',(#1799,#1800,#1801,#1802));
#653=EDGE_LOOP('',(#1803,#1804,#1805,#1806));
#654=EDGE_LOOP('',(#1807,#1808,#1809,#1810));
#655=EDGE_LOOP('',(#1811,#1812,#1813,#1814));
#656=EDGE_LOOP('',(#1815,#1816,#1817,#1818,#1819,#1820));
#657=EDGE_LOOP('',(#1821,#1822,#1823,#1824,#1825,#1826));
#822=LINE('',#3924,#945);
#823=LINE('',#3928,#946);
#824=LINE('',#3932,#947);
#825=LINE('',#3939,#948);
#826=LINE('',#3943,#949);
#827=LINE('',#3947,#950);
#828=LINE('',#3952,#951);
#829=LINE('',#3954,#952);
#830=LINE('',#3956,#953);
#831=LINE('',#3957,#954);
#832=LINE('',#3960,#955);
#833=LINE('',#3962,#956);
#834=LINE('',#3963,#957);
#835=LINE('',#3966,#958);
#836=LINE('',#3968,#959);
#837=LINE('',#3969,#960);
#838=LINE('',#3972,#961);
#839=LINE('',#3974,#962);
#840=LINE('',#3975,#963);
#841=LINE('',#3978,#964);
#842=LINE('',#3980,#965);
#843=LINE('',#3981,#966);
#844=LINE('',#3983,#967);
#845=LINE('',#3984,#968);
#945=VECTOR('',#3117,0.625);
#946=VECTOR('',#3122,0.65);
#947=VECTOR('',#3127,0.635);
#948=VECTOR('',#3136,0.41);
#949=VECTOR('',#3141,0.4);
#950=VECTOR('',#3146,0.36);
#951=VECTOR('',#3151,1.);
#952=VECTOR('',#3152,1.);
#953=VECTOR('',#3153,1.);
#954=VECTOR('',#3154,1.);
#955=VECTOR('',#3157,1.);
#956=VECTOR('',#3158,1.);
#957=VECTOR('',#3159,1.);
#958=VECTOR('',#3162,1.);
#959=VECTOR('',#3163,1.);
#960=VECTOR('',#3164,1.);
#961=VECTOR('',#3167,1.);
#962=VECTOR('',#3168,1.);
#963=VECTOR('',#3169,1.);
#964=VECTOR('',#3172,1.);
#965=VECTOR('',#3173,1.);
#966=VECTOR('',#3174,1.);
#967=VECTOR('',#3177,1.);
#968=VECTOR('',#3178,1.);
#1047=CIRCLE('',#2646,0.6);
#1048=CIRCLE('',#2648,0.65);
#1049=CIRCLE('',#2650,0.65);
#1050=CIRCLE('',#2652,0.62);
#1051=CIRCLE('',#2654,0.42);
#1052=CIRCLE('',#2656,0.3933);
#1053=CIRCLE('',#2658,0.3933);
#1054=CIRCLE('',#2660,0.32);
#1207=VERTEX_POINT('',#3919);
#1208=VERTEX_POINT('',#3922);
#1209=VERTEX_POINT('',#3926);
#1210=VERTEX_POINT('',#3930);
#1211=VERTEX_POINT('',#3934);
#1212=VERTEX_POINT('',#3937);
#1213=VERTEX_POINT('',#3941);
#1214=VERTEX_POINT('',#3945);
#1215=VERTEX_POINT('',#3950);
#1216=VERTEX_POINT('',#3951);
#1217=VERTEX_POINT('',#3953);
#1218=VERTEX_POINT('',#3955);
#1219=VERTEX_POINT('',#3959);
#1220=VERTEX_POINT('',#3961);
#1221=VERTEX_POINT('',#3965);
#1222=VERTEX_POINT('',#3967);
#1223=VERTEX_POINT('',#3971);
#1224=VERTEX_POINT('',#3973);
#1225=VERTEX_POINT('',#3977);
#1226=VERTEX_POINT('',#3979);
#1419=EDGE_CURVE('',#1207,#1207,#1047,.T.);
#1420=EDGE_CURVE('',#1208,#1208,#1048,.T.);
#1421=EDGE_CURVE('',#1208,#1207,#822,.T.);
#1422=EDGE_CURVE('',#1209,#1209,#1049,.T.);
#1423=EDGE_CURVE('',#1209,#1208,#823,.T.);
#1424=EDGE_CURVE('',#1210,#1210,#1050,.T.);
#1425=EDGE_CURVE('',#1210,#1209,#824,.T.);
#1426=EDGE_CURVE('',#1211,#1211,#1051,.T.);
#1427=EDGE_CURVE('',#1212,#1212,#1052,.F.);
#1428=EDGE_CURVE('',#1212,#1211,#825,.T.);
#1429=EDGE_CURVE('',#1213,#1213,#1053,.F.);
#1430=EDGE_CURVE('',#1213,#1212,#826,.T.);
#1431=EDGE_CURVE('',#1214,#1214,#1054,.T.);
#1432=EDGE_CURVE('',#1214,#1213,#827,.T.);
#1433=EDGE_CURVE('',#1215,#1216,#828,.T.);
#1434=EDGE_CURVE('',#1216,#1217,#829,.T.);
#1435=EDGE_CURVE('',#1217,#1218,#830,.T.);
#1436=EDGE_CURVE('',#1215,#1218,#831,.T.);
#1437=EDGE_CURVE('',#1216,#1219,#832,.T.);
#1438=EDGE_CURVE('',#1219,#1220,#833,.T.);
#1439=EDGE_CURVE('',#1220,#1217,#834,.T.);
#1440=EDGE_CURVE('',#1219,#1221,#835,.T.);
#1441=EDGE_CURVE('',#1221,#1222,#836,.T.);
#1442=EDGE_CURVE('',#1222,#1220,#837,.T.);
#1443=EDGE_CURVE('',#1221,#1223,#838,.T.);
#1444=EDGE_CURVE('',#1223,#1224,#839,.T.);
#1445=EDGE_CURVE('',#1224,#1222,#840,.T.);
#1446=EDGE_CURVE('',#1223,#1225,#841,.T.);
#1447=EDGE_CURVE('',#1225,#1226,#842,.T.);
#1448=EDGE_CURVE('',#1226,#1224,#843,.T.);
#1449=EDGE_CURVE('',#1225,#1215,#844,.T.);
#1450=EDGE_CURVE('',#1218,#1226,#845,.T.);
#1763=ORIENTED_EDGE('',*,*,#1419,.F.);
#1764=ORIENTED_EDGE('',*,*,#1420,.F.);
#1765=ORIENTED_EDGE('',*,*,#1421,.T.);
#1766=ORIENTED_EDGE('',*,*,#1419,.T.);
#1767=ORIENTED_EDGE('',*,*,#1421,.F.);
#1768=ORIENTED_EDGE('',*,*,#1422,.F.);
#1769=ORIENTED_EDGE('',*,*,#1423,.T.);
#1770=ORIENTED_EDGE('',*,*,#1420,.T.);
#1771=ORIENTED_EDGE('',*,*,#1423,.F.);
#1772=ORIENTED_EDGE('',*,*,#1424,.F.);
#1773=ORIENTED_EDGE('',*,*,#1425,.T.);
#1774=ORIENTED_EDGE('',*,*,#1422,.T.);
#1775=ORIENTED_EDGE('',*,*,#1425,.F.);
#1776=ORIENTED_EDGE('',*,*,#1424,.T.);
#1777=ORIENTED_EDGE('',*,*,#1426,.F.);
#1778=ORIENTED_EDGE('',*,*,#1427,.F.);
#1779=ORIENTED_EDGE('',*,*,#1428,.T.);
#1780=ORIENTED_EDGE('',*,*,#1426,.T.);
#1781=ORIENTED_EDGE('',*,*,#1428,.F.);
#1782=ORIENTED_EDGE('',*,*,#1429,.F.);
#1783=ORIENTED_EDGE('',*,*,#1430,.T.);
#1784=ORIENTED_EDGE('',*,*,#1427,.T.);
#1785=ORIENTED_EDGE('',*,*,#1430,.F.);
#1786=ORIENTED_EDGE('',*,*,#1431,.F.);
#1787=ORIENTED_EDGE('',*,*,#1432,.T.);
#1788=ORIENTED_EDGE('',*,*,#1429,.T.);
#1789=ORIENTED_EDGE('',*,*,#1432,.F.);
#1790=ORIENTED_EDGE('',*,*,#1431,.T.);
#1791=ORIENTED_EDGE('',*,*,#1433,.T.);
#1792=ORIENTED_EDGE('',*,*,#1434,.T.);
#1793=ORIENTED_EDGE('',*,*,#1435,.T.);
#1794=ORIENTED_EDGE('',*,*,#1436,.F.);
#1795=ORIENTED_EDGE('',*,*,#1437,.T.);
#1796=ORIENTED_EDGE('',*,*,#1438,.T.);
#1797=ORIENTED_EDGE('',*,*,#1439,.T.);
#1798=ORIENTED_EDGE('',*,*,#1434,.F.);
#1799=ORIENTED_EDGE('',*,*,#1440,.T.);
#1800=ORIENTED_EDGE('',*,*,#1441,.T.);
#1801=ORIENTED_EDGE('',*,*,#1442,.T.);
#1802=ORIENTED_EDGE('',*,*,#1438,.F.);
#1803=ORIENTED_EDGE('',*,*,#1443,.T.);
#1804=ORIENTED_EDGE('',*,*,#1444,.T.);
#1805=ORIENTED_EDGE('',*,*,#1445,.T.);
#1806=ORIENTED_EDGE('',*,*,#1441,.F.);
#1807=ORIENTED_EDGE('',*,*,#1446,.T.);
#1808=ORIENTED_EDGE('',*,*,#1447,.T.);
#1809=ORIENTED_EDGE('',*,*,#1448,.T.);
#1810=ORIENTED_EDGE('',*,*,#1444,.F.);
#1811=ORIENTED_EDGE('',*,*,#1449,.T.);
#1812=ORIENTED_EDGE('',*,*,#1436,.T.);
#1813=ORIENTED_EDGE('',*,*,#1450,.T.);
#1814=ORIENTED_EDGE('',*,*,#1447,.F.);
#1815=ORIENTED_EDGE('',*,*,#1449,.F.);
#1816=ORIENTED_EDGE('',*,*,#1446,.F.);
#1817=ORIENTED_EDGE('',*,*,#1443,.F.);
#1818=ORIENTED_EDGE('',*,*,#1440,.F.);
#1819=ORIENTED_EDGE('',*,*,#1437,.F.);
#1820=ORIENTED_EDGE('',*,*,#1433,.F.);
#1821=ORIENTED_EDGE('',*,*,#1450,.F.);
#1822=ORIENTED_EDGE('',*,*,#1435,.F.);
#1823=ORIENTED_EDGE('',*,*,#1439,.F.);
#1824=ORIENTED_EDGE('',*,*,#1442,.F.);
#1825=ORIENTED_EDGE('',*,*,#1445,.F.);
#1826=ORIENTED_EDGE('',*,*,#1448,.F.);
#2187=CYLINDRICAL_SURFACE('',#2649,0.65);
#2188=CYLINDRICAL_SURFACE('',#2657,0.3933);
#2253=ADVANCED_FACE('',(#477),#388,.T.);
#2254=ADVANCED_FACE('',(#478),#231,.T.);
#2255=ADVANCED_FACE('',(#479),#2187,.T.);
#2256=ADVANCED_FACE('',(#480),#232,.T.);
#2257=ADVANCED_FACE('',(#481,#340),#389,.T.);
#2258=ADVANCED_FACE('',(#482),#233,.T.);
#2259=ADVANCED_FACE('',(#483),#2188,.T.);
#2260=ADVANCED_FACE('',(#484),#234,.T.);
#2261=ADVANCED_FACE('',(#485),#390,.T.);
#2262=ADVANCED_FACE('',(#486),#391,.F.);
#2263=ADVANCED_FACE('',(#487),#392,.F.);
#2264=ADVANCED_FACE('',(#488),#393,.F.);
#2265=ADVANCED_FACE('',(#489),#394,.F.);
#2266=ADVANCED_FACE('',(#490),#395,.F.);
#2267=ADVANCED_FACE('',(#491),#396,.F.);
#2268=ADVANCED_FACE('',(#492),#397,.F.);
#2269=ADVANCED_FACE('',(#493),#398,.F.);
#2369=CLOSED_SHELL('',(#2253,#2254,#2255,#2256,#2257,#2258,#2259,#2260,
#2261));
#2370=CLOSED_SHELL('',(#2262,#2263,#2264,#2265,#2266,#2267,#2268,#2269));
#2644=AXIS2_PLACEMENT_3D('',#3917,#3107,#3108);
#2645=AXIS2_PLACEMENT_3D('',#3918,#3109,#3110);
#2646=AXIS2_PLACEMENT_3D('',#3920,#3111,#3112);
#2647=AXIS2_PLACEMENT_3D('',#3921,#3113,#3114);
#2648=AXIS2_PLACEMENT_3D('',#3923,#3115,#3116);
#2649=AXIS2_PLACEMENT_3D('',#3925,#3118,#3119);
#2650=AXIS2_PLACEMENT_3D('',#3927,#3120,#3121);
#2651=AXIS2_PLACEMENT_3D('',#3929,#3123,#3124);
#2652=AXIS2_PLACEMENT_3D('',#3931,#3125,#3126);
#2653=AXIS2_PLACEMENT_3D('',#3933,#3128,#3129);
#2654=AXIS2_PLACEMENT_3D('',#3935,#3130,#3131);
#2655=AXIS2_PLACEMENT_3D('',#3936,#3132,#3133);
#2656=AXIS2_PLACEMENT_3D('',#3938,#3134,#3135);
#2657=AXIS2_PLACEMENT_3D('',#3940,#3137,#3138);
#2658=AXIS2_PLACEMENT_3D('',#3942,#3139,#3140);
#2659=AXIS2_PLACEMENT_3D('',#3944,#3142,#3143);
#2660=AXIS2_PLACEMENT_3D('',#3946,#3144,#3145);
#2661=AXIS2_PLACEMENT_3D('',#3948,#3147,#3148);
#2662=AXIS2_PLACEMENT_3D('',#3949,#3149,#3150);
#2663=AXIS2_PLACEMENT_3D('',#3958,#3155,#3156);
#2664=AXIS2_PLACEMENT_3D('',#3964,#3160,#3161);
#2665=AXIS2_PLACEMENT_3D('',#3970,#3165,#3166);
#2666=AXIS2_PLACEMENT_3D('',#3976,#3170,#3171);
#2667=AXIS2_PLACEMENT_3D('',#3982,#3175,#3176);
#2668=AXIS2_PLACEMENT_3D('',#3985,#3179,#3180);
#2669=AXIS2_PLACEMENT_3D('',#3986,#3181,#3182);
#3107=DIRECTION('axis',(0.,0.,1.));
#3108=DIRECTION('refdir',(1.,0.,0.));
#3109=DIRECTION('center_axis',(0.,1.,0.));
#3110=DIRECTION('ref_axis',(0.,0.,1.));
#3111=DIRECTION('center_axis',(0.,-1.,0.));
#3112=DIRECTION('ref_axis',(1.,0.,0.));
#3113=DIRECTION('center_axis',(0.,-1.,0.));
#3114=DIRECTION('ref_axis',(1.,0.,0.));
#3115=DIRECTION('center_axis',(0.,-1.,0.));
#3116=DIRECTION('ref_axis',(1.,0.,0.));
#3117=DIRECTION('',(0.707106781186548,0.707106781186547,8.65956056235493E-17));
#3118=DIRECTION('center_axis',(0.,-1.,0.));
#3119=DIRECTION('ref_axis',(1.,0.,0.));
#3120=DIRECTION('center_axis',(0.,-1.,0.));
#3121=DIRECTION('ref_axis',(1.,0.,0.));
#3122=DIRECTION('',(0.,1.,0.));
#3123=DIRECTION('center_axis',(0.,1.,0.));
#3124=DIRECTION('ref_axis',(1.,0.,0.));
#3125=DIRECTION('center_axis',(0.,-1.,0.));
#3126=DIRECTION('ref_axis',(1.,0.,0.));
#3127=DIRECTION('',(-0.707106781186548,0.707106781186547,-8.65956056235494E-17));
#3128=DIRECTION('center_axis',(0.,-1.,0.));
#3129=DIRECTION('ref_axis',(0.,0.,-1.));
#3130=DIRECTION('center_axis',(0.,-1.,0.));
#3131=DIRECTION('ref_axis',(1.,0.,0.));
#3132=DIRECTION('center_axis',(0.,1.,0.));
#3133=DIRECTION('ref_axis',(1.,0.,0.));
#3134=DIRECTION('center_axis',(0.,1.,0.));
#3135=DIRECTION('ref_axis',(1.,0.,0.));
#3136=DIRECTION('',(-0.447213595499958,0.894427190999916,-5.47678698264203E-17));
#3137=DIRECTION('center_axis',(0.,-1.,0.));
#3138=DIRECTION('ref_axis',(1.,0.,0.));
#3139=DIRECTION('center_axis',(0.,1.,0.));
#3140=DIRECTION('ref_axis',(1.,0.,0.));
#3141=DIRECTION('',(0.,1.,0.));
#3142=DIRECTION('center_axis',(0.,1.,0.));
#3143=DIRECTION('ref_axis',(1.,0.,0.));
#3144=DIRECTION('center_axis',(0.,-1.,0.));
#3145=DIRECTION('ref_axis',(1.,0.,0.));
#3146=DIRECTION('',(-0.707106781186547,0.707106781186548,-8.65956056235493E-17));
#3147=DIRECTION('center_axis',(0.,-1.,0.));
#3148=DIRECTION('ref_axis',(0.,0.,-1.));
#3149=DIRECTION('center_axis',(0.866025403784439,0.,-0.5));
#3150=DIRECTION('ref_axis',(0.5,0.,0.866025403784439));
#3151=DIRECTION('',(-0.5,0.,-0.866025403784439));
#3152=DIRECTION('',(0.,-1.,0.));
#3153=DIRECTION('',(0.5,0.,0.866025403784439));
#3154=DIRECTION('',(0.,-1.,0.));
#3155=DIRECTION('center_axis',(1.60246890531964E-16,0.,-1.));
#3156=DIRECTION('ref_axis',(1.,0.,1.60246890531964E-16));
#3157=DIRECTION('',(-1.,0.,-1.60246890531964E-16));
#3158=DIRECTION('',(0.,-1.,0.));
#3159=DIRECTION('',(1.,0.,1.60246890531964E-16));
#3160=DIRECTION('center_axis',(-0.866025403784439,0.,-0.5));
#3161=DIRECTION('ref_axis',(0.5,0.,-0.866025403784439));
#3162=DIRECTION('',(-0.5,0.,0.866025403784439));
#3163=DIRECTION('',(0.,-1.,0.));
#3164=DIRECTION('',(0.5,0.,-0.866025403784439));
#3165=DIRECTION('center_axis',(-0.866025403784439,0.,0.5));
#3166=DIRECTION('ref_axis',(-0.5,0.,-0.866025403784439));
#3167=DIRECTION('',(0.5,0.,0.866025403784439));
#3168=DIRECTION('',(0.,-1.,0.));
#3169=DIRECTION('',(-0.5,0.,-0.866025403784439));
#3170=DIRECTION('center_axis',(-1.60246890531964E-16,0.,1.));
#3171=DIRECTION('ref_axis',(-1.,0.,-1.60246890531964E-16));
#3172=DIRECTION('',(1.,0.,1.60246890531964E-16));
#3173=DIRECTION('',(0.,-1.,0.));
#3174=DIRECTION('',(-1.,0.,-1.60246890531964E-16));
#3175=DIRECTION('center_axis',(0.866025403784439,0.,0.5));
#3176=DIRECTION('ref_axis',(-0.5,0.,0.866025403784439));
#3177=DIRECTION('',(0.5,0.,-0.866025403784439));
#3178=DIRECTION('',(-0.5,0.,0.866025403784439));
#3179=DIRECTION('center_axis',(0.,1.,0.));
#3180=DIRECTION('ref_axis',(1.,0.,0.));
#3181=DIRECTION('center_axis',(0.,-1.,0.));
#3182=DIRECTION('ref_axis',(0.,0.,-1.));
#3917=CARTESIAN_POINT('',(0.,0.,0.));
#3918=CARTESIAN_POINT('Origin',(0.6,0.8,0.));
#3919=CARTESIAN_POINT('',(-0.6,0.8,-7.34788079488412E-17));
#3920=CARTESIAN_POINT('Origin',(0.,0.8,0.));
#3921=CARTESIAN_POINT('Origin',(0.,0.775,0.));
#3922=CARTESIAN_POINT('',(-0.65,0.75,-7.9602041944578E-17));
#3923=CARTESIAN_POINT('Origin',(0.,0.75,0.));
#3924=CARTESIAN_POINT('',(-0.625,0.775,-7.65404249467096E-17));
#3925=CARTESIAN_POINT('Origin',(0.,0.39,0.));
#3926=CARTESIAN_POINT('',(-0.65,0.0299999999999998,-7.9602041944578E-17));
#3927=CARTESIAN_POINT('Origin',(0.,0.0299999999999998,0.));
#3928=CARTESIAN_POINT('',(-0.65,0.39,-7.9602041944578E-17));
#3929=CARTESIAN_POINT('Origin',(0.,0.0150000000000001,0.));
#3930=CARTESIAN_POINT('',(-0.62,5.89805981832114E-17,-7.59281015471359E-17));
#3931=CARTESIAN_POINT('Origin',(0.,0.,0.));
#3932=CARTESIAN_POINT('',(-0.635,0.0150000000000001,-7.77650717458569E-17));
#3933=CARTESIAN_POINT('Origin',(0.42,0.,0.));
#3934=CARTESIAN_POINT('',(-0.42,-3.46944695195361E-18,-5.14351655641888E-17));
#3935=CARTESIAN_POINT('Origin',(0.,0.,0.));
#3936=CARTESIAN_POINT('Origin',(0.,-0.02,0.));
#3937=CARTESIAN_POINT('',(-0.3933,-0.0534000000000001,4.81653586104654E-17));
#3938=CARTESIAN_POINT('Origin',(0.,-0.0534000000000001,0.));
#3939=CARTESIAN_POINT('',(-0.41,-0.02,-5.02105187650415E-17));
#3940=CARTESIAN_POINT('Origin',(0.,-1.48,0.));
#3941=CARTESIAN_POINT('',(-0.3933,-2.9267,4.81653586104654E-17));
#3942=CARTESIAN_POINT('Origin',(0.,-2.9267,0.));
#3943=CARTESIAN_POINT('',(-0.3933,-1.48,-4.81653586104654E-17));
#3944=CARTESIAN_POINT('Origin',(0.,-2.96,0.));
#3945=CARTESIAN_POINT('',(-0.32,-3.,-3.91886975727153E-17));
#3946=CARTESIAN_POINT('Origin',(0.,-3.,0.));
#3947=CARTESIAN_POINT('',(-0.36,-2.96,-4.40872847693047E-17));
#3948=CARTESIAN_POINT('Origin',(0.,-3.,0.));
#3949=CARTESIAN_POINT('Origin',(0.173205080756888,-0.8,-0.3));
#3950=CARTESIAN_POINT('',(0.346410161513775,-0.8,0.));
#3951=CARTESIAN_POINT('',(0.173205080756888,-0.8,-0.3));
#3952=CARTESIAN_POINT('',(0.346410161513775,-0.8,0.));
#3953=CARTESIAN_POINT('',(0.173205080756888,-1.28,-0.3));
#3954=CARTESIAN_POINT('',(0.173205080756888,-0.8,-0.3));
#3955=CARTESIAN_POINT('',(0.346410161513775,-1.28,0.));
#3956=CARTESIAN_POINT('',(0.346410161513775,-1.28,0.));
#3957=CARTESIAN_POINT('',(0.346410161513775,-0.8,0.));
#3958=CARTESIAN_POINT('Origin',(-0.173205080756888,-0.8,-0.3));
#3959=CARTESIAN_POINT('',(-0.173205080756888,-0.8,-0.3));
#3960=CARTESIAN_POINT('',(0.173205080756888,-0.8,-0.3));
#3961=CARTESIAN_POINT('',(-0.173205080756888,-1.28,-0.3));
#3962=CARTESIAN_POINT('',(-0.173205080756888,-0.8,-0.3));
#3963=CARTESIAN_POINT('',(0.173205080756888,-1.28,-0.3));
#3964=CARTESIAN_POINT('Origin',(-0.346410161513775,-0.8,-5.55111512312578E-17));
#3965=CARTESIAN_POINT('',(-0.346410161513775,-0.8,-4.24230095489963E-17));
#3966=CARTESIAN_POINT('',(-0.173205080756888,-0.8,-0.3));
#3967=CARTESIAN_POINT('',(-0.346410161513775,-1.28,-5.55111512312578E-17));
#3968=CARTESIAN_POINT('',(-0.346410161513775,-0.8,-4.24230095489963E-17));
#3969=CARTESIAN_POINT('',(-0.173205080756888,-1.28,-0.3));
#3970=CARTESIAN_POINT('Origin',(-0.173205080756888,-0.8,0.3));
#3971=CARTESIAN_POINT('',(-0.173205080756888,-0.8,0.3));
#3972=CARTESIAN_POINT('',(-0.346410161513775,-0.8,-4.24230095489963E-17));
#3973=CARTESIAN_POINT('',(-0.173205080756888,-1.28,0.3));
#3974=CARTESIAN_POINT('',(-0.173205080756888,-0.8,0.3));
#3975=CARTESIAN_POINT('',(-0.346410161513775,-1.28,-4.24230095489963E-17));
#3976=CARTESIAN_POINT('Origin',(0.173205080756888,-0.8,0.3));
#3977=CARTESIAN_POINT('',(0.173205080756888,-0.8,0.3));
#3978=CARTESIAN_POINT('',(-0.173205080756888,-0.8,0.3));
#3979=CARTESIAN_POINT('',(0.173205080756888,-1.28,0.3));
#3980=CARTESIAN_POINT('',(0.173205080756888,-0.8,0.3));
#3981=CARTESIAN_POINT('',(-0.173205080756888,-1.28,0.3));
#3982=CARTESIAN_POINT('Origin',(0.346410161513775,-0.8,0.));
#3983=CARTESIAN_POINT('',(0.173205080756888,-0.8,0.3));
#3984=CARTESIAN_POINT('',(0.173205080756888,-1.28,0.3));
#3985=CARTESIAN_POINT('Origin',(0.,-0.8,-5.55111512312578E-17));
#3986=CARTESIAN_POINT('Origin',(0.,-1.28,-5.55111512312578E-17));
#4740=UNCERTAINTY_MEASURE_WITH_UNIT(LENGTH_MEASURE(0.001),#4778,
'DISTANCE_ACCURACY_VALUE',
'Maximum model space distance between geometric entities at asserted c
onnectivities');
#4755=UNCERTAINTY_MEASURE_WITH_UNIT(LENGTH_MEASURE(0.001),#4778,
'DISTANCE_ACCURACY_VALUE',
'Maximum model space distance between geometric entities at asserted c
onnectivities');
#4762=(
GEOMETRIC_REPRESENTATION_CONTEXT(3)
GLOBAL_UNCERTAINTY_ASSIGNED_CONTEXT((#4740))
GLOBAL_UNIT_ASSIGNED_CONTEXT((#4778,#4780,#4781))
REPRESENTATION_CONTEXT('','3D')
);
#4777=(
GEOMETRIC_REPRESENTATION_CONTEXT(3)
GLOBAL_UNCERTAINTY_ASSIGNED_CONTEXT((#4755))
GLOBAL_UNIT_ASSIGNED_CONTEXT((#4778,#4780,#4781))
REPRESENTATION_CONTEXT('','3D')
);
#4778=(
LENGTH_UNIT()
NAMED_UNIT(*)
SI_UNIT(.CENTI.,.METRE.)
);
#4780=(
NAMED_UNIT(*)
PLANE_ANGLE_UNIT()
SI_UNIT($,.RADIAN.)
);
#4781=(
NAMED_UNIT(*)
SI_UNIT($,.STERADIAN.)
SOLID_ANGLE_UNIT()
);
#4788=SHAPE_DEFINITION_REPRESENTATION(#4809,#4877);
#4809=PRODUCT_DEFINITION_SHAPE('',$,#4899);
#4877=SHAPE_REPRESENTATION('',(#2644),#4762);
#4892=PRODUCT_DEFINITION_CONTEXT('part definition',#4957,'design');
#4899=PRODUCT_DEFINITION('Cap Screw - M8x30','Cap Screw - M8x30',#4920,
#4892);
#4920=PRODUCT_DEFINITION_FORMATION('',$,#4965);
#4957=APPLICATION_CONTEXT(
'Core Data for Automotive Mechanical Design Process');
#4958=PRODUCT_CONTEXT('part definition',#4957,'mechanical');
#4965=PRODUCT('Cap Screw - M8x30','Cap Screw - M8x30',
'Cap Screw - M8x30',(#4958));
#5057=COLOUR_RGB('Black',0.12,0.14,0.17);
#5058=FILL_AREA_STYLE_COLOUR('',#5057);
#5059=FILL_AREA_STYLE('',(#5058));
#5060=SURFACE_STYLE_FILL_AREA(#5059);
#5061=SURFACE_SIDE_STYLE('',(#5060));
#5062=SURFACE_STYLE_USAGE(.BOTH.,#5061);
#5063=PRESENTATION_STYLE_ASSIGNMENT((#5062));
ENDSEC;
END-ISO-10303-21;
